ISO-10303-21;
HEADER;
/* Generated by software containing ST-Developer
 * from STEP Tools, Inc. (www.steptools.com) 
 */

FILE_DESCRIPTION(
/* description */ ('Bin tilter linkage'),
/* implementation_level */ '2;1');

FILE_NAME(
/* name */ 'Pivot keeper (1).step',
/* time_stamp */ '2026-10-28T03:26:24-07:00',
/* author */ (''),
/* organization */ (''),
/* preprocessor_version */ 'ST-DEVELOPER v20.2',
/* originating_system */ 'Autodesk Translation Framework v15.17.0.0',
/* authorisation */ '');

FILE_SCHEMA (('AUTOMOTIVE_DESIGN { 1 0 10303 214 3 1 1 }'));
ENDSEC;

DATA;
#10=MECHANICAL_DESIGN_GEOMETRIC_PRESENTATION_REPRESENTATION('',(#874),#23728);
#662=SHAPE_REPRESENTATION_RELATIONSHIP('SRR','None',#24126,#768);
#768=ADVANCED_BREP_SHAPE_REPRESENTATION('',(#988),#23626);
#874=STYLED_ITEM('',(#24779),#988);
#988=MANIFOLD_SOLID_BREP('Body1',#12404);
#1171=FACE_BOUND('',#2864,.T.);
#1172=FACE_BOUND('',#2866,.T.);
#1550=PLANE('',#13911);
#1551=PLANE('',#13912);
#2000=FACE_OUTER_BOUND('',#2861,.T.);
#2001=FACE_OUTER_BOUND('',#2862,.T.);
#2002=FACE_OUTER_BOUND('',#2863,.T.);
#2003=FACE_OUTER_BOUND('',#2865,.T.);
#2861=EDGE_LOOP('',(#8853,#8854,#8855,#8856));
#2862=EDGE_LOOP('',(#8857,#8858,#8859,#8860));
#2863=EDGE_LOOP('',(#8861));
#2864=EDGE_LOOP('',(#8862));
#2865=EDGE_LOOP('',(#8863));
#2866=EDGE_LOOP('',(#8864));
#3985=LINE('',#20274,#4660);
#3986=LINE('',#20280,#4661);
#4660=VECTOR('',#16072,0.225000000000001);
#4661=VECTOR('',#16079,1.);
#5303=CIRCLE('',#13906,0.225000000000001);
#5304=CIRCLE('',#13907,0.225000000000001);
#5305=CIRCLE('',#13909,1.);
#5306=CIRCLE('',#13910,1.);
#6117=VERTEX_POINT('',#20271);
#6118=VERTEX_POINT('',#20273);
#6119=VERTEX_POINT('',#20277);
#6120=VERTEX_POINT('',#20279);
#7166=EDGE_CURVE('',#6117,#6117,#5303,.T.);
#7167=EDGE_CURVE('',#6117,#6118,#3985,.T.);
#7168=EDGE_CURVE('',#6118,#6118,#5304,.T.);
#7169=EDGE_CURVE('',#6119,#6119,#5305,.T.);
#7170=EDGE_CURVE('',#6119,#6120,#3986,.T.);
#7171=EDGE_CURVE('',#6120,#6120,#5306,.T.);
#8853=ORIENTED_EDGE('',*,*,#7166,.F.);
#8854=ORIENTED_EDGE('',*,*,#7167,.T.);
#8855=ORIENTED_EDGE('',*,*,#7168,.T.);
#8856=ORIENTED_EDGE('',*,*,#7167,.F.);
#8857=ORIENTED_EDGE('',*,*,#7169,.F.);
#8858=ORIENTED_EDGE('',*,*,#7170,.T.);
#8859=ORIENTED_EDGE('',*,*,#7171,.T.);
#8860=ORIENTED_EDGE('',*,*,#7170,.F.);
#8861=ORIENTED_EDGE('',*,*,#7169,.T.);
#8862=ORIENTED_EDGE('',*,*,#7166,.T.);
#8863=ORIENTED_EDGE('',*,*,#7171,.F.);
#8864=ORIENTED_EDGE('',*,*,#7168,.F.);
#11319=CYLINDRICAL_SURFACE('',#13905,0.225000000000001);
#11320=CYLINDRICAL_SURFACE('',#13908,1.);
#11725=ADVANCED_FACE('',(#2000),#11319,.F.);
#11726=ADVANCED_FACE('',(#2001),#11320,.T.);
#11727=ADVANCED_FACE('',(#2002,#1171),#1550,.T.);
#11728=ADVANCED_FACE('',(#2003,#1172),#1551,.F.);
#12404=CLOSED_SHELL('',(#11725,#11726,#11727,#11728));
#13904=AXIS2_PLACEMENT_3D('',#20269,#16066,#16067);
#13905=AXIS2_PLACEMENT_3D('',#20270,#16068,#16069);
#13906=AXIS2_PLACEMENT_3D('',#20272,#16070,#16071);
#13907=AXIS2_PLACEMENT_3D('',#20275,#16073,#16074);
#13908=AXIS2_PLACEMENT_3D('',#20276,#16075,#16076);
#13909=AXIS2_PLACEMENT_3D('',#20278,#16077,#16078);
#13910=AXIS2_PLACEMENT_3D('',#20281,#16080,#16081);
#13911=AXIS2_PLACEMENT_3D('',#20282,#16082,#16083);
#13912=AXIS2_PLACEMENT_3D('',#20283,#16084,#16085);
#16066=DIRECTION('axis',(0.,0.,1.));
#16067=DIRECTION('refdir',(1.,0.,0.));
#16068=DIRECTION('center_axis',(0.,1.,0.));
#16069=DIRECTION('ref_axis',(1.,0.,0.));
#16070=DIRECTION('center_axis',(0.,-1.,0.));
#16071=DIRECTION('ref_axis',(1.,0.,0.));
#16072=DIRECTION('',(0.,-1.,0.));
#16073=DIRECTION('center_axis',(0.,-1.,0.));
#16074=DIRECTION('ref_axis',(1.,0.,0.));
#16075=DIRECTION('center_axis',(0.,1.,0.));
#16076=DIRECTION('ref_axis',(1.,0.,0.));
#16077=DIRECTION('center_axis',(0.,1.,0.));
#16078=DIRECTION('ref_axis',(1.,0.,0.));
#16079=DIRECTION('',(0.,-1.,0.));
#16080=DIRECTION('center_axis',(0.,1.,0.));
#16081=DIRECTION('ref_axis',(1.,0.,0.));
#16082=DIRECTION('center_axis',(0.,1.,0.));
#16083=DIRECTION('ref_axis',(1.,0.,0.));
#16084=DIRECTION('center_axis',(0.,1.,0.));
#16085=DIRECTION('ref_axis',(1.,0.,0.));
#20269=CARTESIAN_POINT('',(0.,0.,0.));
#20270=CARTESIAN_POINT('Origin',(18.,-1.2,15.));
#20271=CARTESIAN_POINT('',(17.775,-1.,15.));
#20272=CARTESIAN_POINT('Origin',(18.,-1.,15.));
#20273=CARTESIAN_POINT('',(17.775,-1.2,15.));
#20274=CARTESIAN_POINT('',(17.775,-1.2,15.));
#20275=CARTESIAN_POINT('Origin',(18.,-1.2,15.));
#20276=CARTESIAN_POINT('Origin',(18.,-1.2,15.));
#20277=CARTESIAN_POINT('',(17.,-1.,15.));
#20278=CARTESIAN_POINT('Origin',(18.,-1.,15.));
#20279=CARTESIAN_POINT('',(17.,-1.2,15.));
#20280=CARTESIAN_POINT('',(17.,-1.2,15.));
#20281=CARTESIAN_POINT('Origin',(18.,-1.2,15.));
#20282=CARTESIAN_POINT('Origin',(18.,-1.,15.));
#20283=CARTESIAN_POINT('Origin',(18.,-1.2,15.));
#23509=UNCERTAINTY_MEASURE_WITH_UNIT(LENGTH_MEASURE(0.001),#23729,
'DISTANCE_ACCURACY_VALUE',
'Maximum model space distance between geometric entities at asserted c
onnectivities');
#23611=UNCERTAINTY_MEASURE_WITH_UNIT(LENGTH_MEASURE(0.001),#23729,
'DISTANCE_ACCURACY_VALUE',
'Maximum model space distance between geometric entities at asserted c
onnectivities');
#23626=(
GEOMETRIC_REPRESENTATION_CONTEXT(3)
GLOBAL_UNCERTAINTY_ASSIGNED_CONTEXT((#23509))
GLOBAL_UNIT_ASSIGNED_CONTEXT((#23729,#23731,#23732))
REPRESENTATION_CONTEXT('','3D')
);
#23728=(
GEOMETRIC_REPRESENTATION_CONTEXT(3)
GLOBAL_UNCERTAINTY_ASSIGNED_CONTEXT((#23611))
GLOBAL_UNIT_ASSIGNED_CONTEXT((#23729,#23731,#23732))
REPRESENTATION_CONTEXT('','3D')
);
#23729=(
LENGTH_UNIT()
NAMED_UNIT(*)
SI_UNIT(.CENTI.,.METRE.)
);
#23731=(
NAMED_UNIT(*)
PLANE_ANGLE_UNIT()
SI_UNIT($,.RADIAN.)
);
#23732=(
NAMED_UNIT(*)
SI_UNIT($,.STERADIAN.)
SOLID_ANGLE_UNIT()
);
#23747=SHAPE_DEFINITION_REPRESENTATION(#23863,#24126);
#23863=PRODUCT_DEFINITION_SHAPE('',$,#24243);
#24126=SHAPE_REPRESENTATION('',(#13904),#23626);
#24228=PRODUCT_DEFINITION_CONTEXT('part definition',#24578,'design');
#24243=PRODUCT_DEFINITION('Pivot keeper (1)','Pivot keeper (1)',#24359,#24228);
#24359=PRODUCT_DEFINITION_FORMATION('',$,#24594);
#24578=APPLICATION_CONTEXT(
'Core Data for Automotive Mechanical Design Process');
#24579=PRODUCT_CONTEXT('part definition',#24578,'mechanical');
#24594=PRODUCT('Pivot keeper (1)','Pivot keeper (1)','Pivot keeper (1)',(#24579));
#24773=COLOUR_RGB('Off White',0.89,0.88,0.83);
#24774=FILL_AREA_STYLE_COLOUR('',#24773);
#24775=FILL_AREA_STYLE('',(#24774));
#24776=SURFACE_STYLE_FILL_AREA(#24775);
#24777=SURFACE_SIDE_STYLE('',(#24776));
#24778=SURFACE_STYLE_USAGE(.BOTH.,#24777);
#24779=PRESENTATION_STYLE_ASSIGNMENT((#24778));
ENDSEC;
END-ISO-10303-21;
